ISO-10303-21;
HEADER;
/* Generated by software containing ST-Developer
 * from STEP Tools, Inc. (www.steptools.com) 
 */

FILE_DESCRIPTION(
/* description */ ('Belt-driven linear axis on 2020 extrusion'),
/* implementation_level */ '2;1');

FILE_NAME(
/* name */ 'Flat Washer - M5.step',
/* time_stamp */ '2026-10-28T03:26:09-07:00',
/* author */ (''),
/* organization */ (''),
/* preprocessor_version */ 'ST-DEVELOPER v20.2',
/* originating_system */ 'Autodesk Translation Framework v15.17.0.0',
/* authorisation */ '');

FILE_SCHEMA (('AUTOMOTIVE_DESIGN { 1 0 10303 214 3 1 1 }'));
ENDSEC;

DATA;
#10=MECHANICAL_DESIGN_GEOMETRIC_PRESENTATION_REPRESENTATION('',(#662),#20096);
#504=CONICAL_SURFACE('',#12602,0.275,0.785398163397449);
#560=SHAPE_REPRESENTATION_RELATIONSHIP('SRR','None',#20361,#606);
#606=ADVANCED_BREP_SHAPE_REPRESENTATION('',(#717),#20092);
#662=STYLED_ITEM('',(#20657),#717);
#717=MANIFOLD_SOLID_BREP('Body1',#10976);
#884=FACE_BOUND('',#2608,.T.);
#885=FACE_BOUND('',#2611,.T.);
#1215=PLANE('',#12607);
#1216=PLANE('',#12611);
#1817=FACE_OUTER_BOUND('',#2605,.T.);
#1818=FACE_OUTER_BOUND('',#2606,.T.);
#1819=FACE_OUTER_BOUND('',#2607,.T.);
#1820=FACE_OUTER_BOUND('',#2609,.T.);
#1821=FACE_OUTER_BOUND('',#2610,.T.);
#2605=EDGE_LOOP('',(#9873,#9874,#9875,#9876));
#2606=EDGE_LOOP('',(#9877,#9878,#9879,#9880));
#2607=EDGE_LOOP('',(#9881));
#2608=EDGE_LOOP('',(#9882));
#2609=EDGE_LOOP('',(#9883,#9884,#9885,#9886));
#2610=EDGE_LOOP('',(#9887));
#2611=EDGE_LOOP('',(#9888));
#3448=LINE('',#19672,#4305);
#3449=LINE('',#19676,#4306);
#3450=LINE('',#19683,#4307);
#4305=VECTOR('',#15796,0.275);
#4306=VECTOR('',#15801,0.265);
#4307=VECTOR('',#15810,0.5);
#4864=CIRCLE('',#12603,0.285);
#4865=CIRCLE('',#12604,0.265);
#4866=CIRCLE('',#12606,0.265);
#4867=CIRCLE('',#12608,0.5);
#4868=CIRCLE('',#12610,0.5);
#5777=VERTEX_POINT('',#19669);
#5778=VERTEX_POINT('',#19671);
#5779=VERTEX_POINT('',#19675);
#5780=VERTEX_POINT('',#19679);
#5781=VERTEX_POINT('',#19682);
#7151=EDGE_CURVE('',#5777,#5777,#4864,.T.);
#7152=EDGE_CURVE('',#5777,#5778,#3448,.T.);
#7153=EDGE_CURVE('',#5778,#5778,#4865,.T.);
#7154=EDGE_CURVE('',#5778,#5779,#3449,.T.);
#7155=EDGE_CURVE('',#5779,#5779,#4866,.T.);
#7156=EDGE_CURVE('',#5780,#5780,#4867,.T.);
#7157=EDGE_CURVE('',#5780,#5781,#3450,.T.);
#7158=EDGE_CURVE('',#5781,#5781,#4868,.T.);
#9873=ORIENTED_EDGE('',*,*,#7151,.T.);
#9874=ORIENTED_EDGE('',*,*,#7152,.T.);
#9875=ORIENTED_EDGE('',*,*,#7153,.T.);
#9876=ORIENTED_EDGE('',*,*,#7152,.F.);
#9877=ORIENTED_EDGE('',*,*,#7153,.F.);
#9878=ORIENTED_EDGE('',*,*,#7154,.T.);
#9879=ORIENTED_EDGE('',*,*,#7155,.T.);
#9880=ORIENTED_EDGE('',*,*,#7154,.F.);
#9881=ORIENTED_EDGE('',*,*,#7156,.T.);
#9882=ORIENTED_EDGE('',*,*,#7151,.F.);
#9883=ORIENTED_EDGE('',*,*,#7156,.F.);
#9884=ORIENTED_EDGE('',*,*,#7157,.T.);
#9885=ORIENTED_EDGE('',*,*,#7158,.T.);
#9886=ORIENTED_EDGE('',*,*,#7157,.F.);
#9887=ORIENTED_EDGE('',*,*,#7158,.F.);
#9888=ORIENTED_EDGE('',*,*,#7155,.F.);
#10293=CYLINDRICAL_SURFACE('',#12605,0.265);
#10294=CYLINDRICAL_SURFACE('',#12609,0.5);
#10868=ADVANCED_FACE('',(#1817),#504,.F.);
#10869=ADVANCED_FACE('',(#1818),#10293,.F.);
#10870=ADVANCED_FACE('',(#1819,#884),#1215,.T.);
#10871=ADVANCED_FACE('',(#1820),#10294,.T.);
#10872=ADVANCED_FACE('',(#1821,#885),#1216,.F.);
#10976=CLOSED_SHELL('',(#10868,#10869,#10870,#10871,#10872));
#12601=AXIS2_PLACEMENT_3D('',#19667,#15790,#15791);
#12602=AXIS2_PLACEMENT_3D('',#19668,#15792,#15793);
#12603=AXIS2_PLACEMENT_3D('',#19670,#15794,#15795);
#12604=AXIS2_PLACEMENT_3D('',#19673,#15797,#15798);
#12605=AXIS2_PLACEMENT_3D('',#19674,#15799,#15800);
#12606=AXIS2_PLACEMENT_3D('',#19677,#15802,#15803);
#12607=AXIS2_PLACEMENT_3D('',#19678,#15804,#15805);
#12608=AXIS2_PLACEMENT_3D('',#19680,#15806,#15807);
#12609=AXIS2_PLACEMENT_3D('',#19681,#15808,#15809);
#12610=AXIS2_PLACEMENT_3D('',#19684,#15811,#15812);
#12611=AXIS2_PLACEMENT_3D('',#19685,#15813,#15814);
#15790=DIRECTION('axis',(0.,0.,1.));
#15791=DIRECTION('refdir',(1.,0.,0.));
#15792=DIRECTION('center_axis',(0.,1.,0.));
#15793=DIRECTION('ref_axis',(1.,0.,0.));
#15794=DIRECTION('center_axis',(0.,1.,0.));
#15795=DIRECTION('ref_axis',(1.,0.,0.));
#15796=DIRECTION('',(0.707106781186548,-0.707106781186547,-8.65956056235494E-17));
#15797=DIRECTION('center_axis',(0.,-1.,0.));
#15798=DIRECTION('ref_axis',(1.,0.,0.));
#15799=DIRECTION('center_axis',(0.,1.,0.));
#15800=DIRECTION('ref_axis',(1.,0.,0.));
#15801=DIRECTION('',(0.,-1.,0.));
#15802=DIRECTION('center_axis',(0.,-1.,0.));
#15803=DIRECTION('ref_axis',(1.,0.,0.));
#15804=DIRECTION('center_axis',(0.,1.,0.));
#15805=DIRECTION('ref_axis',(1.,0.,0.));
#15806=DIRECTION('center_axis',(0.,1.,0.));
#15807=DIRECTION('ref_axis',(1.,0.,0.));
#15808=DIRECTION('center_axis',(0.,1.,0.));
#15809=DIRECTION('ref_axis',(1.,0.,0.));
#15810=DIRECTION('',(0.,-1.,0.));
#15811=DIRECTION('center_axis',(0.,1.,0.));
#15812=DIRECTION('ref_axis',(1.,0.,0.));
#15813=DIRECTION('center_axis',(0.,1.,0.));
#15814=DIRECTION('ref_axis',(1.,0.,0.));
#19667=CARTESIAN_POINT('',(0.,0.,0.));
#19668=CARTESIAN_POINT('Origin',(0.,0.09,0.));
#19669=CARTESIAN_POINT('',(-0.285,0.1,3.49024337756996E-17));
#19670=CARTESIAN_POINT('Origin',(0.,0.1,0.));
#19671=CARTESIAN_POINT('',(-0.265,0.08,-3.24531401774049E-17));
#19672=CARTESIAN_POINT('',(-0.275,0.09,3.36777869765522E-17));
#19673=CARTESIAN_POINT('Origin',(0.,0.08,0.));
#19674=CARTESIAN_POINT('Origin',(0.,0.,0.));
#19675=CARTESIAN_POINT('',(-0.265,0.,3.24531401774049E-17));
#19676=CARTESIAN_POINT('',(-0.265,0.,3.24531401774049E-17));
#19677=CARTESIAN_POINT('Origin',(0.,0.,0.));
#19678=CARTESIAN_POINT('Origin',(0.,0.1,0.));
#19679=CARTESIAN_POINT('',(-0.5,0.1,6.12323399573677E-17));
#19680=CARTESIAN_POINT('Origin',(0.,0.1,0.));
#19681=CARTESIAN_POINT('Origin',(0.,0.,0.));
#19682=CARTESIAN_POINT('',(-0.5,0.,6.12323399573677E-17));
#19683=CARTESIAN_POINT('',(-0.5,0.,6.12323399573677E-17));
#19684=CARTESIAN_POINT('Origin',(0.,0.,0.));
#19685=CARTESIAN_POINT('Origin',(0.,0.,0.));
#20038=UNCERTAINTY_MEASURE_WITH_UNIT(LENGTH_MEASURE(0.001),#20097,
'DISTANCE_ACCURACY_VALUE',
'Maximum model space distance between geometric entities at asserted c
onnectivities');
#20042=UNCERTAINTY_MEASURE_WITH_UNIT(LENGTH_MEASURE(0.001),#20097,
'DISTANCE_ACCURACY_VALUE',
'Maximum model space distance between geometric entities at asserted c
onnectivities');
#20092=(
GEOMETRIC_REPRESENTATION_CONTEXT(3)
GLOBAL_UNCERTAINTY_ASSIGNED_CONTEXT((#20038))
GLOBAL_UNIT_ASSIGNED_CONTEXT((#20097,#20099,#20100))
REPRESENTATION_CONTEXT('','3D')
);
#20096=(
GEOMETRIC_REPRESENTATION_CONTEXT(3)
GLOBAL_UNCERTAINTY_ASSIGNED_CONTEXT((#20042))
GLOBAL_UNIT_ASSIGNED_CONTEXT((#20097,#20099,#20100))
REPRESENTATION_CONTEXT('','3D')
);
#20097=(
LENGTH_UNIT()
NAMED_UNIT(*)
SI_UNIT(.CENTI.,.METRE.)
);
#20099=(
NAMED_UNIT(*)
PLANE_ANGLE_UNIT()
SI_UNIT($,.RADIAN.)
);
#20100=(
NAMED_UNIT(*)
SI_UNIT($,.STERADIAN.)
SOLID_ANGLE_UNIT()
);
#20150=SHAPE_DEFINITION_REPRESENTATION(#20211,#20361);
#20211=PRODUCT_DEFINITION_SHAPE('',$,#20415);
#20361=SHAPE_REPRESENTATION('',(#12601),#20092);
#20365=PRODUCT_DEFINITION_CONTEXT('part definition',#20526,'design');
#20415=PRODUCT_DEFINITION('Flat Washer - M5','Flat Washer - M5',#20468,
#20365);
#20468=PRODUCT_DEFINITION_FORMATION('',$,#20577);
#20526=APPLICATION_CONTEXT(
'Core Data for Automotive Mechanical Design Process');
#20527=PRODUCT_CONTEXT('part definition',#20526,'mechanical');
#20577=PRODUCT('Flat Washer - M5','Flat Washer - M5','Flat Washer - M5',
(#20527));
#20651=COLOUR_RGB('Black',0.12,0.14,0.17);
#20652=FILL_AREA_STYLE_COLOUR('',#20651);
#20653=FILL_AREA_STYLE('',(#20652));
#20654=SURFACE_STYLE_FILL_AREA(#20653);
#20655=SURFACE_SIDE_STYLE('',(#20654));
#20656=SURFACE_STYLE_USAGE(.BOTH.,#20655);
#20657=PRESENTATION_STYLE_ASSIGNMENT((#20656));
ENDSEC;
END-ISO-10303-21;
